ISO-10303-21;
HEADER;
/* Generated by software containing ST-Developer
 * from STEP Tools, Inc. (www.steptools.com) 
 */

FILE_DESCRIPTION(
/* description */ ('Bin tilter linkage'),
/* implementation_level */ '2;1');

FILE_NAME(
/* name */ 'Screw bearing keeper.step',
/* time_stamp */ '2026-10-28T03:26:24-07:00',
/* author */ (''),
/* organization */ (''),
/* preprocessor_version */ 'ST-DEVELOPER v20.2',
/* originating_system */ 'Autodesk Translation Framework v15.17.0.0',
/* authorisation */ '');

FILE_SCHEMA (('AUTOMOTIVE_DESIGN { 1 0 10303 214 3 1 1 }'));
ENDSEC;

DATA;
#10=MECHANICAL_DESIGN_GEOMETRIC_PRESENTATION_REPRESENTATION('',(#876),#23728);
#664=SHAPE_REPRESENTATION_RELATIONSHIP('SRR','None',#24128,#770);
#770=ADVANCED_BREP_SHAPE_REPRESENTATION('',(#990),#23628);
#876=STYLED_ITEM('',(#24772),#990);
#990=MANIFOLD_SOLID_BREP('Body1',#12406);
#1187=FACE_BOUND('',#2904,.T.);
#1188=FACE_BOUND('',#2905,.T.);
#1189=FACE_BOUND('',#2906,.T.);
#1190=FACE_BOUND('',#2911,.T.);
#1191=FACE_BOUND('',#2912,.T.);
#1192=FACE_BOUND('',#2913,.T.);
#1561=PLANE('',#13963);
#1562=PLANE('',#13973);
#2022=FACE_OUTER_BOUND('',#2899,.T.);
#2023=FACE_OUTER_BOUND('',#2900,.T.);
#2024=FACE_OUTER_BOUND('',#2901,.T.);
#2025=FACE_OUTER_BOUND('',#2902,.T.);
#2026=FACE_OUTER_BOUND('',#2903,.T.);
#2027=FACE_OUTER_BOUND('',#2907,.T.);
#2028=FACE_OUTER_BOUND('',#2908,.T.);
#2029=FACE_OUTER_BOUND('',#2909,.T.);
#2030=FACE_OUTER_BOUND('',#2910,.T.);
#2899=EDGE_LOOP('',(#8949,#8950,#8951,#8952));
#2900=EDGE_LOOP('',(#8953,#8954,#8955,#8956));
#2901=EDGE_LOOP('',(#8957,#8958,#8959,#8960));
#2902=EDGE_LOOP('',(#8961,#8962,#8963,#8964));
#2903=EDGE_LOOP('',(#8965,#8966,#8967,#8968));
#2904=EDGE_LOOP('',(#8969));
#2905=EDGE_LOOP('',(#8970));
#2906=EDGE_LOOP('',(#8971));
#2907=EDGE_LOOP('',(#8972,#8973,#8974,#8975));
#2908=EDGE_LOOP('',(#8976,#8977,#8978,#8979));
#2909=EDGE_LOOP('',(#8980,#8981,#8982,#8983));
#2910=EDGE_LOOP('',(#8984,#8985,#8986,#8987));
#2911=EDGE_LOOP('',(#8988));
#2912=EDGE_LOOP('',(#8989));
#2913=EDGE_LOOP('',(#8990));
#4011=LINE('',#20378,#4686);
#4012=LINE('',#20384,#4687);
#4013=LINE('',#20389,#4688);
#4014=LINE('',#20393,#4689);
#4015=LINE('',#20398,#4690);
#4016=LINE('',#20402,#4691);
#4017=LINE('',#20415,#4692);
#4686=VECTOR('',#16190,0.225);
#4687=VECTOR('',#16197,0.225);
#4688=VECTOR('',#16202,1.);
#4689=VECTOR('',#16205,1.);
#4690=VECTOR('',#16210,1.);
#4691=VECTOR('',#16213,1.);
#4692=VECTOR('',#16234,1.02);
#5325=CIRCLE('',#13952,0.225);
#5326=CIRCLE('',#13953,0.225);
#5327=CIRCLE('',#13955,0.225);
#5328=CIRCLE('',#13956,0.225);
#5329=CIRCLE('',#13958,0.61);
#5330=CIRCLE('',#13959,0.61);
#5331=CIRCLE('',#13961,0.61);
#5332=CIRCLE('',#13962,0.61);
#5333=CIRCLE('',#13964,2.1);
#5334=CIRCLE('',#13965,2.1);
#5335=CIRCLE('',#13966,1.02);
#5336=CIRCLE('',#13968,2.1);
#5337=CIRCLE('',#13970,2.1);
#5338=CIRCLE('',#13972,1.02);
#6149=VERTEX_POINT('',#20375);
#6150=VERTEX_POINT('',#20377);
#6151=VERTEX_POINT('',#20381);
#6152=VERTEX_POINT('',#20383);
#6153=VERTEX_POINT('',#20387);
#6154=VERTEX_POINT('',#20388);
#6155=VERTEX_POINT('',#20390);
#6156=VERTEX_POINT('',#20392);
#6157=VERTEX_POINT('',#20396);
#6158=VERTEX_POINT('',#20397);
#6159=VERTEX_POINT('',#20399);
#6160=VERTEX_POINT('',#20401);
#6161=VERTEX_POINT('',#20407);
#6162=VERTEX_POINT('',#20414);
#7214=EDGE_CURVE('',#6149,#6149,#5325,.T.);
#7215=EDGE_CURVE('',#6149,#6150,#4011,.T.);
#7216=EDGE_CURVE('',#6150,#6150,#5326,.T.);
#7217=EDGE_CURVE('',#6151,#6151,#5327,.T.);
#7218=EDGE_CURVE('',#6151,#6152,#4012,.T.);
#7219=EDGE_CURVE('',#6152,#6152,#5328,.T.);
#7220=EDGE_CURVE('',#6153,#6154,#4013,.T.);
#7221=EDGE_CURVE('',#6155,#6153,#5329,.T.);
#7222=EDGE_CURVE('',#6156,#6155,#4014,.T.);
#7223=EDGE_CURVE('',#6154,#6156,#5330,.T.);
#7224=EDGE_CURVE('',#6157,#6158,#4015,.T.);
#7225=EDGE_CURVE('',#6159,#6157,#5331,.T.);
#7226=EDGE_CURVE('',#6160,#6159,#4016,.T.);
#7227=EDGE_CURVE('',#6158,#6160,#5332,.T.);
#7228=EDGE_CURVE('',#6153,#6159,#5333,.T.);
#7229=EDGE_CURVE('',#6157,#6155,#5334,.T.);
#7230=EDGE_CURVE('',#6161,#6161,#5335,.T.);
#7231=EDGE_CURVE('',#6154,#6160,#5336,.T.);
#7232=EDGE_CURVE('',#6158,#6156,#5337,.T.);
#7233=EDGE_CURVE('',#6161,#6162,#4017,.T.);
#7234=EDGE_CURVE('',#6162,#6162,#5338,.T.);
#8949=ORIENTED_EDGE('',*,*,#7214,.F.);
#8950=ORIENTED_EDGE('',*,*,#7215,.T.);
#8951=ORIENTED_EDGE('',*,*,#7216,.F.);
#8952=ORIENTED_EDGE('',*,*,#7215,.F.);
#8953=ORIENTED_EDGE('',*,*,#7217,.F.);
#8954=ORIENTED_EDGE('',*,*,#7218,.T.);
#8955=ORIENTED_EDGE('',*,*,#7219,.F.);
#8956=ORIENTED_EDGE('',*,*,#7218,.F.);
#8957=ORIENTED_EDGE('',*,*,#7220,.F.);
#8958=ORIENTED_EDGE('',*,*,#7221,.F.);
#8959=ORIENTED_EDGE('',*,*,#7222,.F.);
#8960=ORIENTED_EDGE('',*,*,#7223,.F.);
#8961=ORIENTED_EDGE('',*,*,#7224,.F.);
#8962=ORIENTED_EDGE('',*,*,#7225,.F.);
#8963=ORIENTED_EDGE('',*,*,#7226,.F.);
#8964=ORIENTED_EDGE('',*,*,#7227,.F.);
#8965=ORIENTED_EDGE('',*,*,#7221,.T.);
#8966=ORIENTED_EDGE('',*,*,#7228,.T.);
#8967=ORIENTED_EDGE('',*,*,#7225,.T.);
#8968=ORIENTED_EDGE('',*,*,#7229,.T.);
#8969=ORIENTED_EDGE('',*,*,#7216,.T.);
#8970=ORIENTED_EDGE('',*,*,#7219,.T.);
#8971=ORIENTED_EDGE('',*,*,#7230,.T.);
#8972=ORIENTED_EDGE('',*,*,#7220,.T.);
#8973=ORIENTED_EDGE('',*,*,#7231,.T.);
#8974=ORIENTED_EDGE('',*,*,#7226,.T.);
#8975=ORIENTED_EDGE('',*,*,#7228,.F.);
#8976=ORIENTED_EDGE('',*,*,#7222,.T.);
#8977=ORIENTED_EDGE('',*,*,#7229,.F.);
#8978=ORIENTED_EDGE('',*,*,#7224,.T.);
#8979=ORIENTED_EDGE('',*,*,#7232,.T.);
#8980=ORIENTED_EDGE('',*,*,#7230,.F.);
#8981=ORIENTED_EDGE('',*,*,#7233,.T.);
#8982=ORIENTED_EDGE('',*,*,#7234,.T.);
#8983=ORIENTED_EDGE('',*,*,#7233,.F.);
#8984=ORIENTED_EDGE('',*,*,#7223,.T.);
#8985=ORIENTED_EDGE('',*,*,#7232,.F.);
#8986=ORIENTED_EDGE('',*,*,#7227,.T.);
#8987=ORIENTED_EDGE('',*,*,#7231,.F.);
#8988=ORIENTED_EDGE('',*,*,#7214,.T.);
#8989=ORIENTED_EDGE('',*,*,#7217,.T.);
#8990=ORIENTED_EDGE('',*,*,#7234,.F.);
#11330=CYLINDRICAL_SURFACE('',#13951,0.225);
#11331=CYLINDRICAL_SURFACE('',#13954,0.225);
#11332=CYLINDRICAL_SURFACE('',#13957,0.61);
#11333=CYLINDRICAL_SURFACE('',#13960,0.61);
#11334=CYLINDRICAL_SURFACE('',#13967,2.1);
#11335=CYLINDRICAL_SURFACE('',#13969,2.1);
#11336=CYLINDRICAL_SURFACE('',#13971,1.02);
#11747=ADVANCED_FACE('',(#2022),#11330,.F.);
#11748=ADVANCED_FACE('',(#2023),#11331,.F.);
#11749=ADVANCED_FACE('',(#2024),#11332,.F.);
#11750=ADVANCED_FACE('',(#2025),#11333,.F.);
#11751=ADVANCED_FACE('',(#2026,#1187,#1188,#1189),#1561,.T.);
#11752=ADVANCED_FACE('',(#2027),#11334,.T.);
#11753=ADVANCED_FACE('',(#2028),#11335,.T.);
#11754=ADVANCED_FACE('',(#2029),#11336,.F.);
#11755=ADVANCED_FACE('',(#2030,#1190,#1191,#1192),#1562,.F.);
#12406=CLOSED_SHELL('',(#11747,#11748,#11749,#11750,#11751,#11752,#11753,
#11754,#11755));
#13950=AXIS2_PLACEMENT_3D('',#20373,#16184,#16185);
#13951=AXIS2_PLACEMENT_3D('',#20374,#16186,#16187);
#13952=AXIS2_PLACEMENT_3D('',#20376,#16188,#16189);
#13953=AXIS2_PLACEMENT_3D('',#20379,#16191,#16192);
#13954=AXIS2_PLACEMENT_3D('',#20380,#16193,#16194);
#13955=AXIS2_PLACEMENT_3D('',#20382,#16195,#16196);
#13956=AXIS2_PLACEMENT_3D('',#20385,#16198,#16199);
#13957=AXIS2_PLACEMENT_3D('',#20386,#16200,#16201);
#13958=AXIS2_PLACEMENT_3D('',#20391,#16203,#16204);
#13959=AXIS2_PLACEMENT_3D('',#20394,#16206,#16207);
#13960=AXIS2_PLACEMENT_3D('',#20395,#16208,#16209);
#13961=AXIS2_PLACEMENT_3D('',#20400,#16211,#16212);
#13962=AXIS2_PLACEMENT_3D('',#20403,#16214,#16215);
#13963=AXIS2_PLACEMENT_3D('',#20404,#16216,#16217);
#13964=AXIS2_PLACEMENT_3D('',#20405,#16218,#16219);
#13965=AXIS2_PLACEMENT_3D('',#20406,#16220,#16221);
#13966=AXIS2_PLACEMENT_3D('',#20408,#16222,#16223);
#13967=AXIS2_PLACEMENT_3D('',#20409,#16224,#16225);
#13968=AXIS2_PLACEMENT_3D('',#20410,#16226,#16227);
#13969=AXIS2_PLACEMENT_3D('',#20411,#16228,#16229);
#13970=AXIS2_PLACEMENT_3D('',#20412,#16230,#16231);
#13971=AXIS2_PLACEMENT_3D('',#20413,#16232,#16233);
#13972=AXIS2_PLACEMENT_3D('',#20416,#16235,#16236);
#13973=AXIS2_PLACEMENT_3D('',#20417,#16237,#16238);
#16184=DIRECTION('axis',(0.,0.,1.));
#16185=DIRECTION('refdir',(1.,0.,0.));
#16186=DIRECTION('center_axis',(1.,0.,0.));
#16187=DIRECTION('ref_axis',(0.,0.,-1.));
#16188=DIRECTION('center_axis',(1.,0.,0.));
#16189=DIRECTION('ref_axis',(0.,0.,-1.));
#16190=DIRECTION('',(1.,0.,0.));
#16191=DIRECTION('center_axis',(-1.,0.,0.));
#16192=DIRECTION('ref_axis',(0.,0.,-1.));
#16193=DIRECTION('center_axis',(1.,0.,0.));
#16194=DIRECTION('ref_axis',(0.,0.,-1.));
#16195=DIRECTION('center_axis',(1.,0.,0.));
#16196=DIRECTION('ref_axis',(0.,0.,-1.));
#16197=DIRECTION('',(1.,0.,0.));
#16198=DIRECTION('center_axis',(-1.,0.,0.));
#16199=DIRECTION('ref_axis',(0.,0.,-1.));
#16200=DIRECTION('center_axis',(1.,0.,0.));
#16201=DIRECTION('ref_axis',(0.,0.,-1.));
#16202=DIRECTION('',(-1.,0.,0.));
#16203=DIRECTION('center_axis',(-1.,0.,0.));
#16204=DIRECTION('ref_axis',(0.,0.,-1.));
#16205=DIRECTION('',(1.,0.,0.));
#16206=DIRECTION('center_axis',(1.,0.,0.));
#16207=DIRECTION('ref_axis',(0.,0.,-1.));
#16208=DIRECTION('center_axis',(1.,0.,0.));
#16209=DIRECTION('ref_axis',(0.,0.,-1.));
#16210=DIRECTION('',(-1.,0.,0.));
#16211=DIRECTION('center_axis',(-1.,0.,0.));
#16212=DIRECTION('ref_axis',(0.,0.,-1.));
#16213=DIRECTION('',(1.,0.,0.));
#16214=DIRECTION('center_axis',(1.,0.,0.));
#16215=DIRECTION('ref_axis',(0.,0.,-1.));
#16216=DIRECTION('center_axis',(1.,0.,0.));
#16217=DIRECTION('ref_axis',(0.,0.,-1.));
#16218=DIRECTION('center_axis',(1.,0.,0.));
#16219=DIRECTION('ref_axis',(0.,0.,-1.));
#16220=DIRECTION('center_axis',(1.,0.,0.));
#16221=DIRECTION('ref_axis',(0.,0.,-1.));
#16222=DIRECTION('center_axis',(-1.,0.,0.));
#16223=DIRECTION('ref_axis',(0.,0.,-1.));
#16224=DIRECTION('center_axis',(1.,0.,0.));
#16225=DIRECTION('ref_axis',(0.,0.,-1.));
#16226=DIRECTION('center_axis',(1.,0.,0.));
#16227=DIRECTION('ref_axis',(0.,0.,-1.));
#16228=DIRECTION('center_axis',(1.,0.,0.));
#16229=DIRECTION('ref_axis',(0.,-1.22464679914735E-16,1.));
#16230=DIRECTION('center_axis',(1.,0.,0.));
#16231=DIRECTION('ref_axis',(0.,0.,-1.));
#16232=DIRECTION('center_axis',(1.,0.,0.));
#16233=DIRECTION('ref_axis',(0.,0.,-1.));
#16234=DIRECTION('',(-1.,0.,0.));
#16235=DIRECTION('center_axis',(-1.,0.,0.));
#16236=DIRECTION('ref_axis',(0.,0.,-1.));
#16237=DIRECTION('center_axis',(1.,0.,0.));
#16238=DIRECTION('ref_axis',(0.,0.,-1.));
#20373=CARTESIAN_POINT('',(0.,0.,0.));
#20374=CARTESIAN_POINT('Origin',(-10.3,-4.5,9.85));
#20375=CARTESIAN_POINT('',(-10.2,-4.5,10.075));
#20376=CARTESIAN_POINT('Origin',(-10.2,-4.5,9.85));
#20377=CARTESIAN_POINT('',(-10.,-4.5,10.075));
#20378=CARTESIAN_POINT('',(-10.3,-4.5,10.075));
#20379=CARTESIAN_POINT('Origin',(-10.,-4.5,9.85));
#20380=CARTESIAN_POINT('Origin',(-10.3,-4.5,6.15));
#20381=CARTESIAN_POINT('',(-10.2,-4.5,6.375));
#20382=CARTESIAN_POINT('Origin',(-10.2,-4.5,6.15));
#20383=CARTESIAN_POINT('',(-10.,-4.5,6.375));
#20384=CARTESIAN_POINT('',(-10.3,-4.5,6.375));
#20385=CARTESIAN_POINT('Origin',(-10.,-4.5,6.15));
#20386=CARTESIAN_POINT('Origin',(-10.3,-7.,8.));
#20387=CARTESIAN_POINT('',(-10.,-6.55758,7.58004221212127));
#20388=CARTESIAN_POINT('',(-10.2,-6.55758,7.58004221212127));
#20389=CARTESIAN_POINT('',(-10.3,-6.55758,7.58004221212127));
#20390=CARTESIAN_POINT('',(-10.,-6.55758,8.41995778787873));
#20391=CARTESIAN_POINT('Origin',(-10.,-7.,8.));
#20392=CARTESIAN_POINT('',(-10.2,-6.55758,8.41995778787873));
#20393=CARTESIAN_POINT('',(-10.3,-6.55758,8.41995778787873));
#20394=CARTESIAN_POINT('Origin',(-10.2,-7.,8.));
#20395=CARTESIAN_POINT('Origin',(-10.3,-2.,8.));
#20396=CARTESIAN_POINT('',(-10.,-2.44242,8.41995778787873));
#20397=CARTESIAN_POINT('',(-10.2,-2.44242,8.41995778787873));
#20398=CARTESIAN_POINT('',(-10.3,-2.44242,8.41995778787873));
#20399=CARTESIAN_POINT('',(-10.,-2.44242,7.58004221212127));
#20400=CARTESIAN_POINT('Origin',(-10.,-2.,8.));
#20401=CARTESIAN_POINT('',(-10.2,-2.44242,7.58004221212127));
#20402=CARTESIAN_POINT('',(-10.3,-2.44242,7.58004221212127));
#20403=CARTESIAN_POINT('Origin',(-10.2,-2.,8.));
#20404=CARTESIAN_POINT('Origin',(-10.,-4.5,8.));
#20405=CARTESIAN_POINT('Origin',(-10.,-4.5,8.));
#20406=CARTESIAN_POINT('Origin',(-10.,-4.5,8.));
#20407=CARTESIAN_POINT('',(-10.,-4.5,9.02));
#20408=CARTESIAN_POINT('Origin',(-10.,-4.5,8.));
#20409=CARTESIAN_POINT('Origin',(-10.2,-4.5,8.));
#20410=CARTESIAN_POINT('Origin',(-10.2,-4.5,8.));
#20411=CARTESIAN_POINT('Origin',(-10.2,-4.5,8.));
#20412=CARTESIAN_POINT('Origin',(-10.2,-4.5,8.));
#20413=CARTESIAN_POINT('Origin',(-10.2,-4.5,8.));
#20414=CARTESIAN_POINT('',(-10.2,-4.5,9.02));
#20415=CARTESIAN_POINT('',(-10.2,-4.5,9.02));
#20416=CARTESIAN_POINT('Origin',(-10.2,-4.5,8.));
#20417=CARTESIAN_POINT('Origin',(-10.2,-4.5,8.));
#23511=UNCERTAINTY_MEASURE_WITH_UNIT(LENGTH_MEASURE(0.001),#23729,
'DISTANCE_ACCURACY_VALUE',
'Maximum model space distance between geometric entities at asserted c
onnectivities');
#23611=UNCERTAINTY_MEASURE_WITH_UNIT(LENGTH_MEASURE(0.001),#23729,
'DISTANCE_ACCURACY_VALUE',
'Maximum model space distance between geometric entities at asserted c
onnectivities');
#23628=(
GEOMETRIC_REPRESENTATION_CONTEXT(3)
GLOBAL_UNCERTAINTY_ASSIGNED_CONTEXT((#23511))
GLOBAL_UNIT_ASSIGNED_CONTEXT((#23729,#23731,#23732))
REPRESENTATION_CONTEXT('','3D')
);
#23728=(
GEOMETRIC_REPRESENTATION_CONTEXT(3)
GLOBAL_UNCERTAINTY_ASSIGNED_CONTEXT((#23611))
GLOBAL_UNIT_ASSIGNED_CONTEXT((#23729,#23731,#23732))
REPRESENTATION_CONTEXT('','3D')
);
#23729=(
LENGTH_UNIT()
NAMED_UNIT(*)
SI_UNIT(.CENTI.,.METRE.)
);
#23731=(
NAMED_UNIT(*)
PLANE_ANGLE_UNIT()
SI_UNIT($,.RADIAN.)
);
#23732=(
NAMED_UNIT(*)
SI_UNIT($,.STERADIAN.)
SOLID_ANGLE_UNIT()
);
#23749=SHAPE_DEFINITION_REPRESENTATION(#23865,#24128);
#23865=PRODUCT_DEFINITION_SHAPE('',$,#24245);
#24128=SHAPE_REPRESENTATION('',(#13950),#23628);
#24228=PRODUCT_DEFINITION_CONTEXT('part definition',#24578,'design');
#24245=PRODUCT_DEFINITION('Screw bearing keeper','Screw bearing keeper',
#24361,#24228);
#24361=PRODUCT_DEFINITION_FORMATION('',$,#24596);
#24578=APPLICATION_CONTEXT(
'Core Data for Automotive Mechanical Design Process');
#24579=PRODUCT_CONTEXT('part definition',#24578,'mechanical');
#24596=PRODUCT('Screw bearing keeper','Screw bearing keeper',
'Screw bearing keeper',(#24579));
#24766=COLOUR_RGB('Black',0.12,0.14,0.17);
#24767=FILL_AREA_STYLE_COLOUR('',#24766);
#24768=FILL_AREA_STYLE('',(#24767));
#24769=SURFACE_STYLE_FILL_AREA(#24768);
#24770=SURFACE_SIDE_STYLE('',(#24769));
#24771=SURFACE_STYLE_USAGE(.BOTH.,#24770);
#24772=PRESENTATION_STYLE_ASSIGNMENT((#24771));
ENDSEC;
END-ISO-10303-21;
